ISO-10303-21;
HEADER;
/* Generated by software containing ST-Developer
 * from STEP Tools, Inc. (www.steptools.com) 
 */

FILE_DESCRIPTION(
/* description */ ('Double-row support with tensioned shaft'),
/* implementation_level */ '2;1');

FILE_NAME(
/* name */ 'Flange hole reducer (4).step',
/* time_stamp */ '2026-10-27T10:50:35-07:00',
/* author */ (''),
/* organization */ (''),
/* preprocessor_version */ 'ST-DEVELOPER v20.2',
/* originating_system */ 'Autodesk Translation Framework v15.17.0.0',
/* authorisation */ '');

FILE_SCHEMA (('AUTOMOTIVE_DESIGN { 1 0 10303 214 3 1 1 }'));
ENDSEC;

DATA;
#10=MECHANICAL_DESIGN_GEOMETRIC_PRESENTATION_REPRESENTATION('',(#490),#11559);
#426=SHAPE_REPRESENTATION_RELATIONSHIP('SRR','None',#11734,#458);
#458=ADVANCED_BREP_SHAPE_REPRESENTATION('',(#523),#11536);
#490=STYLED_ITEM('',(#11981),#523);
#523=MANIFOLD_SOLID_BREP('Body1',#6335);
#602=FACE_BOUND('',#1412,.T.);
#603=FACE_BOUND('',#1414,.T.);
#733=PLANE('',#6889);
#734=PLANE('',#6890);
#1005=FACE_OUTER_BOUND('',#1409,.T.);
#1006=FACE_OUTER_BOUND('',#1410,.T.);
#1007=FACE_OUTER_BOUND('',#1411,.T.);
#1008=FACE_OUTER_BOUND('',#1413,.T.);
#1409=EDGE_LOOP('',(#4726,#4727,#4728,#4729));
#1410=EDGE_LOOP('',(#4730,#4731,#4732,#4733));
#1411=EDGE_LOOP('',(#4734));
#1412=EDGE_LOOP('',(#4735));
#1413=EDGE_LOOP('',(#4736));
#1414=EDGE_LOOP('',(#4737));
#1872=LINE('',#9670,#2419);
#1873=LINE('',#9676,#2420);
#2419=VECTOR('',#7845,0.425);
#2420=VECTOR('',#7852,0.595);
#2904=CIRCLE('',#6884,0.425);
#2905=CIRCLE('',#6885,0.425);
#2906=CIRCLE('',#6887,0.595);
#2907=CIRCLE('',#6888,0.595);
#3159=VERTEX_POINT('',#9667);
#3160=VERTEX_POINT('',#9669);
#3161=VERTEX_POINT('',#9673);
#3162=VERTEX_POINT('',#9675);
#3748=EDGE_CURVE('',#3159,#3159,#2904,.T.);
#3749=EDGE_CURVE('',#3159,#3160,#1872,.T.);
#3750=EDGE_CURVE('',#3160,#3160,#2905,.T.);
#3751=EDGE_CURVE('',#3161,#3161,#2906,.T.);
#3752=EDGE_CURVE('',#3161,#3162,#1873,.T.);
#3753=EDGE_CURVE('',#3162,#3162,#2907,.T.);
#4726=ORIENTED_EDGE('',*,*,#3748,.F.);
#4727=ORIENTED_EDGE('',*,*,#3749,.T.);
#4728=ORIENTED_EDGE('',*,*,#3750,.T.);
#4729=ORIENTED_EDGE('',*,*,#3749,.F.);
#4730=ORIENTED_EDGE('',*,*,#3751,.F.);
#4731=ORIENTED_EDGE('',*,*,#3752,.T.);
#4732=ORIENTED_EDGE('',*,*,#3753,.T.);
#4733=ORIENTED_EDGE('',*,*,#3752,.F.);
#4734=ORIENTED_EDGE('',*,*,#3751,.T.);
#4735=ORIENTED_EDGE('',*,*,#3748,.T.);
#4736=ORIENTED_EDGE('',*,*,#3753,.F.);
#4737=ORIENTED_EDGE('',*,*,#3750,.F.);
#5924=CYLINDRICAL_SURFACE('',#6883,0.425);
#5925=CYLINDRICAL_SURFACE('',#6886,0.595);
#6068=ADVANCED_FACE('',(#1005),#5924,.F.);
#6069=ADVANCED_FACE('',(#1006),#5925,.T.);
#6070=ADVANCED_FACE('',(#1007,#602),#733,.T.);
#6071=ADVANCED_FACE('',(#1008,#603),#734,.F.);
#6335=CLOSED_SHELL('',(#6068,#6069,#6070,#6071));
#6882=AXIS2_PLACEMENT_3D('',#9665,#7839,#7840);
#6883=AXIS2_PLACEMENT_3D('',#9666,#7841,#7842);
#6884=AXIS2_PLACEMENT_3D('',#9668,#7843,#7844);
#6885=AXIS2_PLACEMENT_3D('',#9671,#7846,#7847);
#6886=AXIS2_PLACEMENT_3D('',#9672,#7848,#7849);
#6887=AXIS2_PLACEMENT_3D('',#9674,#7850,#7851);
#6888=AXIS2_PLACEMENT_3D('',#9677,#7853,#7854);
#6889=AXIS2_PLACEMENT_3D('',#9678,#7855,#7856);
#6890=AXIS2_PLACEMENT_3D('',#9679,#7857,#7858);
#7839=DIRECTION('axis',(0.,0.,1.));
#7840=DIRECTION('refdir',(1.,0.,0.));
#7841=DIRECTION('center_axis',(0.,1.,0.));
#7842=DIRECTION('ref_axis',(1.,0.,0.));
#7843=DIRECTION('center_axis',(0.,-1.,0.));
#7844=DIRECTION('ref_axis',(1.,0.,0.));
#7845=DIRECTION('',(0.,-1.,0.));
#7846=DIRECTION('center_axis',(0.,-1.,0.));
#7847=DIRECTION('ref_axis',(1.,0.,0.));
#7848=DIRECTION('center_axis',(0.,1.,0.));
#7849=DIRECTION('ref_axis',(1.,0.,0.));
#7850=DIRECTION('center_axis',(0.,1.,0.));
#7851=DIRECTION('ref_axis',(1.,0.,0.));
#7852=DIRECTION('',(0.,-1.,0.));
#7853=DIRECTION('center_axis',(0.,1.,0.));
#7854=DIRECTION('ref_axis',(1.,0.,0.));
#7855=DIRECTION('center_axis',(0.,1.,0.));
#7856=DIRECTION('ref_axis',(1.,0.,0.));
#7857=DIRECTION('center_axis',(0.,1.,0.));
#7858=DIRECTION('ref_axis',(1.,0.,0.));
#9665=CARTESIAN_POINT('',(0.,0.,0.));
#9666=CARTESIAN_POINT('Origin',(-3.2,17.5,6.8));
#9667=CARTESIAN_POINT('',(-3.625,18.5,6.8));
#9668=CARTESIAN_POINT('Origin',(-3.2,18.5,6.8));
#9669=CARTESIAN_POINT('',(-3.625,17.5,6.8));
#9670=CARTESIAN_POINT('',(-3.625,17.5,6.8));
#9671=CARTESIAN_POINT('Origin',(-3.2,17.5,6.8));
#9672=CARTESIAN_POINT('Origin',(-3.2,17.5,6.8));
#9673=CARTESIAN_POINT('',(-3.795,18.5,6.8));
#9674=CARTESIAN_POINT('Origin',(-3.2,18.5,6.8));
#9675=CARTESIAN_POINT('',(-3.795,17.5,6.8));
#9676=CARTESIAN_POINT('',(-3.795,17.5,6.8));
#9677=CARTESIAN_POINT('Origin',(-3.2,17.5,6.8));
#9678=CARTESIAN_POINT('Origin',(-3.2,18.5,6.8));
#9679=CARTESIAN_POINT('Origin',(-3.2,17.5,6.8));
#11499=UNCERTAINTY_MEASURE_WITH_UNIT(LENGTH_MEASURE(0.001),#11560,
'DISTANCE_ACCURACY_VALUE',
'Maximum model space distance between geometric entities at asserted c
onnectivities');
#11522=UNCERTAINTY_MEASURE_WITH_UNIT(LENGTH_MEASURE(0.001),#11560,
'DISTANCE_ACCURACY_VALUE',
'Maximum model space distance between geometric entities at asserted c
onnectivities');
#11536=(
GEOMETRIC_REPRESENTATION_CONTEXT(3)
GLOBAL_UNCERTAINTY_ASSIGNED_CONTEXT((#11499))
GLOBAL_UNIT_ASSIGNED_CONTEXT((#11560,#11562,#11563))
REPRESENTATION_CONTEXT('','3D')
);
#11559=(
GEOMETRIC_REPRESENTATION_CONTEXT(3)
GLOBAL_UNCERTAINTY_ASSIGNED_CONTEXT((#11522))
GLOBAL_UNIT_ASSIGNED_CONTEXT((#11560,#11562,#11563))
REPRESENTATION_CONTEXT('','3D')
);
#11560=(
LENGTH_UNIT()
NAMED_UNIT(*)
SI_UNIT(.CENTI.,.METRE.)
);
#11562=(
NAMED_UNIT(*)
PLANE_ANGLE_UNIT()
SI_UNIT($,.RADIAN.)
);
#11563=(
NAMED_UNIT(*)
SI_UNIT($,.STERADIAN.)
SOLID_ANGLE_UNIT()
);
#11577=SHAPE_DEFINITION_REPRESENTATION(#11613,#11734);
#11613=PRODUCT_DEFINITION_SHAPE('',$,#11771);
#11734=SHAPE_REPRESENTATION('',(#6882),#11536);
#11757=PRODUCT_DEFINITION_CONTEXT('part definition',#11867,'design');
#11771=PRODUCT_DEFINITION('Flange hole reducer (4)',
'Flange hole reducer (4)',#11807,#11757);
#11807=PRODUCT_DEFINITION_FORMATION('',$,#11882);
#11867=APPLICATION_CONTEXT(
'Core Data for Automotive Mechanical Design Process');
#11868=PRODUCT_CONTEXT('part definition',#11867,'mechanical');
#11882=PRODUCT('Flange hole reducer (4)','Flange hole reducer (4)',
'Flange hole reducer (4)',(#11868));
#11975=COLOUR_RGB('Off White',0.89,0.88,0.83);
#11976=FILL_AREA_STYLE_COLOUR('',#11975);
#11977=FILL_AREA_STYLE('',(#11976));
#11978=SURFACE_STYLE_FILL_AREA(#11977);
#11979=SURFACE_SIDE_STYLE('',(#11978));
#11980=SURFACE_STYLE_USAGE(.BOTH.,#11979);
#11981=PRESENTATION_STYLE_ASSIGNMENT((#11980));
ENDSEC;
END-ISO-10303-21;
